ISO-10303-21;
HEADER;
/* Generated by software containing ST-Developer
 * from STEP Tools, Inc. (www.steptools.com) 
 */

FILE_DESCRIPTION(
/* description */ ('Jaw-coupled motor to shaft test stand'),
/* implementation_level */ '2;1');

FILE_NAME(
/* name */ 'M5x14 Cap Screw.step',
/* time_stamp */ '2026-10-27T10:46:06-07:00',
/* author */ (''),
/* organization */ (''),
/* preprocessor_version */ 'ST-DEVELOPER v20.2',
/* originating_system */ 'Autodesk Translation Framework v15.17.0.0',
/* authorisation */ '');

FILE_SCHEMA (('AUTOMOTIVE_DESIGN { 1 0 10303 214 3 1 1 }'));
ENDSEC;

DATA;
#10=MECHANICAL_DESIGN_GEOMETRIC_PRESENTATION_REPRESENTATION('',(#358),#19361);
#14=CONICAL_SURFACE('',#11706,0.4,0.785398163397448);
#15=CONICAL_SURFACE('',#11710,0.41,0.785398163397448);
#16=CONICAL_SURFACE('',#11714,0.26,0.463647609000806);
#30=ORIENTED_CLOSED_SHELL('',*,#11003,.F.);
#33=BREP_WITH_VOIDS('Body1',#11004,(#30));
#293=SHAPE_REPRESENTATION_RELATIONSHIP('SRR','None',#19508,#325);
#325=ADVANCED_BREP_SHAPE_REPRESENTATION('',(#33),#19344);
#358=STYLED_ITEM('',(#19753),#33);
#482=FACE_BOUND('',#1920,.T.);
#641=PLANE('',#11694);
#642=PLANE('',#11695);
#643=PLANE('',#11696);
#644=PLANE('',#11697);
#645=PLANE('',#11698);
#646=PLANE('',#11699);
#647=PLANE('',#11700);
#648=PLANE('',#11701);
#649=PLANE('',#11702);
#650=PLANE('',#11704);
#651=PLANE('',#11712);
#1207=FACE_OUTER_BOUND('',#1906,.T.);
#1208=FACE_OUTER_BOUND('',#1907,.T.);
#1209=FACE_OUTER_BOUND('',#1908,.T.);
#1210=FACE_OUTER_BOUND('',#1909,.T.);
#1211=FACE_OUTER_BOUND('',#1910,.T.);
#1212=FACE_OUTER_BOUND('',#1911,.T.);
#1213=FACE_OUTER_BOUND('',#1912,.T.);
#1214=FACE_OUTER_BOUND('',#1913,.T.);
#1215=FACE_OUTER_BOUND('',#1914,.T.);
#1216=FACE_OUTER_BOUND('',#1915,.T.);
#1217=FACE_OUTER_BOUND('',#1916,.T.);
#1218=FACE_OUTER_BOUND('',#1917,.T.);
#1219=FACE_OUTER_BOUND('',#1918,.T.);
#1220=FACE_OUTER_BOUND('',#1919,.T.);
#1221=FACE_OUTER_BOUND('',#1921,.T.);
#1222=FACE_OUTER_BOUND('',#1922,.T.);
#1906=EDGE_LOOP('',(#8152,#8153,#8154,#8155));
#1907=EDGE_LOOP('',(#8156,#8157,#8158,#8159));
#1908=EDGE_LOOP('',(#8160,#8161,#8162,#8163));
#1909=EDGE_LOOP('',(#8164,#8165,#8166,#8167));
#1910=EDGE_LOOP('',(#8168,#8169,#8170,#8171));
#1911=EDGE_LOOP('',(#8172,#8173,#8174,#8175));
#1912=EDGE_LOOP('',(#8176,#8177,#8178,#8179,#8180,#8181));
#1913=EDGE_LOOP('',(#8182,#8183,#8184,#8185,#8186,#8187));
#1914=EDGE_LOOP('',(#8188));
#1915=EDGE_LOOP('',(#8189));
#1916=EDGE_LOOP('',(#8190,#8191,#8192,#8193));
#1917=EDGE_LOOP('',(#8194,#8195,#8196,#8197));
#1918=EDGE_LOOP('',(#8198,#8199,#8200,#8201));
#1919=EDGE_LOOP('',(#8202));
#1920=EDGE_LOOP('',(#8203));
#1921=EDGE_LOOP('',(#8204,#8205,#8206,#8207));
#1922=EDGE_LOOP('',(#8208,#8209,#8210,#8211));
#2641=LINE('',#16724,#3794);
#2642=LINE('',#16726,#3795);
#2643=LINE('',#16728,#3796);
#2644=LINE('',#16729,#3797);
#2645=LINE('',#16732,#3798);
#2646=LINE('',#16734,#3799);
#2647=LINE('',#16735,#3800);
#2648=LINE('',#16738,#3801);
#2649=LINE('',#16740,#3802);
#2650=LINE('',#16741,#3803);
#2651=LINE('',#16744,#3804);
#2652=LINE('',#16746,#3805);
#2653=LINE('',#16747,#3806);
#2654=LINE('',#16750,#3807);
#2655=LINE('',#16752,#3808);
#2656=LINE('',#16753,#3809);
#2657=LINE('',#16755,#3810);
#2658=LINE('',#16756,#3811);
#2659=LINE('',#16768,#3812);
#2660=LINE('',#16772,#3813);
#2661=LINE('',#16776,#3814);
#2662=LINE('',#16783,#3815);
#2663=LINE('',#16785,#3816);
#3794=VECTOR('',#13250,1.);
#3795=VECTOR('',#13251,1.);
#3796=VECTOR('',#13252,1.);
#3797=VECTOR('',#13253,1.);
#3798=VECTOR('',#13256,1.);
#3799=VECTOR('',#13257,1.);
#3800=VECTOR('',#13258,1.);
#3801=VECTOR('',#13261,1.);
#3802=VECTOR('',#13262,1.);
#3803=VECTOR('',#13263,1.);
#3804=VECTOR('',#13266,1.);
#3805=VECTOR('',#13267,1.);
#3806=VECTOR('',#13268,1.);
#3807=VECTOR('',#13271,1.);
#3808=VECTOR('',#13272,1.);
#3809=VECTOR('',#13273,1.);
#3810=VECTOR('',#13276,1.);
#3811=VECTOR('',#13277,1.);
#3812=VECTOR('',#13294,0.4);
#3813=VECTOR('',#13299,0.425);
#3814=VECTOR('',#13304,0.41);
#3815=VECTOR('',#13313,0.26);
#3816=VECTOR('',#13316,0.25);
#4794=CIRCLE('',#11703,0.24505);
#4795=CIRCLE('',#11705,0.375);
#4796=CIRCLE('',#11707,0.425);
#4797=CIRCLE('',#11709,0.425);
#4798=CIRCLE('',#11711,0.395);
#4799=CIRCLE('',#11713,0.27);
#4800=CIRCLE('',#11715,0.24505);
#5218=VERTEX_POINT('',#16722);
#5219=VERTEX_POINT('',#16723);
#5220=VERTEX_POINT('',#16725);
#5221=VERTEX_POINT('',#16727);
#5222=VERTEX_POINT('',#16731);
#5223=VERTEX_POINT('',#16733);
#5224=VERTEX_POINT('',#16737);
#5225=VERTEX_POINT('',#16739);
#5226=VERTEX_POINT('',#16743);
#5227=VERTEX_POINT('',#16745);
#5228=VERTEX_POINT('',#16749);
#5229=VERTEX_POINT('',#16751);
#5230=VERTEX_POINT('',#16760);
#5231=VERTEX_POINT('',#16763);
#5232=VERTEX_POINT('',#16766);
#5233=VERTEX_POINT('',#16770);
#5234=VERTEX_POINT('',#16774);
#5235=VERTEX_POINT('',#16778);
#5236=VERTEX_POINT('',#16781);
#6287=EDGE_CURVE('',#5218,#5219,#2641,.T.);
#6288=EDGE_CURVE('',#5219,#5220,#2642,.T.);
#6289=EDGE_CURVE('',#5220,#5221,#2643,.T.);
#6290=EDGE_CURVE('',#5218,#5221,#2644,.T.);
#6291=EDGE_CURVE('',#5219,#5222,#2645,.T.);
#6292=EDGE_CURVE('',#5222,#5223,#2646,.T.);
#6293=EDGE_CURVE('',#5223,#5220,#2647,.T.);
#6294=EDGE_CURVE('',#5222,#5224,#2648,.T.);
#6295=EDGE_CURVE('',#5224,#5225,#2649,.T.);
#6296=EDGE_CURVE('',#5225,#5223,#2650,.T.);
#6297=EDGE_CURVE('',#5224,#5226,#2651,.T.);
#6298=EDGE_CURVE('',#5226,#5227,#2652,.T.);
#6299=EDGE_CURVE('',#5227,#5225,#2653,.T.);
#6300=EDGE_CURVE('',#5226,#5228,#2654,.T.);
#6301=EDGE_CURVE('',#5228,#5229,#2655,.T.);
#6302=EDGE_CURVE('',#5229,#5227,#2656,.T.);
#6303=EDGE_CURVE('',#5228,#5218,#2657,.T.);
#6304=EDGE_CURVE('',#5221,#5229,#2658,.T.);
#6305=EDGE_CURVE('',#5230,#5230,#4794,.T.);
#6306=EDGE_CURVE('',#5231,#5231,#4795,.T.);
#6307=EDGE_CURVE('',#5232,#5232,#4796,.T.);
#6308=EDGE_CURVE('',#5232,#5231,#2659,.T.);
#6309=EDGE_CURVE('',#5233,#5233,#4797,.T.);
#6310=EDGE_CURVE('',#5233,#5232,#2660,.T.);
#6311=EDGE_CURVE('',#5234,#5234,#4798,.T.);
#6312=EDGE_CURVE('',#5234,#5233,#2661,.T.);
#6313=EDGE_CURVE('',#5235,#5235,#4799,.T.);
#6314=EDGE_CURVE('',#5236,#5236,#4800,.F.);
#6315=EDGE_CURVE('',#5236,#5235,#2662,.T.);
#6316=EDGE_CURVE('',#5230,#5236,#2663,.T.);
#8152=ORIENTED_EDGE('',*,*,#6287,.T.);
#8153=ORIENTED_EDGE('',*,*,#6288,.T.);
#8154=ORIENTED_EDGE('',*,*,#6289,.T.);
#8155=ORIENTED_EDGE('',*,*,#6290,.F.);
#8156=ORIENTED_EDGE('',*,*,#6291,.T.);
#8157=ORIENTED_EDGE('',*,*,#6292,.T.);
#8158=ORIENTED_EDGE('',*,*,#6293,.T.);
#8159=ORIENTED_EDGE('',*,*,#6288,.F.);
#8160=ORIENTED_EDGE('',*,*,#6294,.T.);
#8161=ORIENTED_EDGE('',*,*,#6295,.T.);
#8162=ORIENTED_EDGE('',*,*,#6296,.T.);
#8163=ORIENTED_EDGE('',*,*,#6292,.F.);
#8164=ORIENTED_EDGE('',*,*,#6297,.T.);
#8165=ORIENTED_EDGE('',*,*,#6298,.T.);
#8166=ORIENTED_EDGE('',*,*,#6299,.T.);
#8167=ORIENTED_EDGE('',*,*,#6295,.F.);
#8168=ORIENTED_EDGE('',*,*,#6300,.T.);
#8169=ORIENTED_EDGE('',*,*,#6301,.T.);
#8170=ORIENTED_EDGE('',*,*,#6302,.T.);
#8171=ORIENTED_EDGE('',*,*,#6298,.F.);
#8172=ORIENTED_EDGE('',*,*,#6303,.T.);
#8173=ORIENTED_EDGE('',*,*,#6290,.T.);
#8174=ORIENTED_EDGE('',*,*,#6304,.T.);
#8175=ORIENTED_EDGE('',*,*,#6301,.F.);
#8176=ORIENTED_EDGE('',*,*,#6303,.F.);
#8177=ORIENTED_EDGE('',*,*,#6300,.F.);
#8178=ORIENTED_EDGE('',*,*,#6297,.F.);
#8179=ORIENTED_EDGE('',*,*,#6294,.F.);
#8180=ORIENTED_EDGE('',*,*,#6291,.F.);
#8181=ORIENTED_EDGE('',*,*,#6287,.F.);
#8182=ORIENTED_EDGE('',*,*,#6304,.F.);
#8183=ORIENTED_EDGE('',*,*,#6289,.F.);
#8184=ORIENTED_EDGE('',*,*,#6293,.F.);
#8185=ORIENTED_EDGE('',*,*,#6296,.F.);
#8186=ORIENTED_EDGE('',*,*,#6299,.F.);
#8187=ORIENTED_EDGE('',*,*,#6302,.F.);
#8188=ORIENTED_EDGE('',*,*,#6305,.F.);
#8189=ORIENTED_EDGE('',*,*,#6306,.F.);
#8190=ORIENTED_EDGE('',*,*,#6307,.F.);
#8191=ORIENTED_EDGE('',*,*,#6308,.T.);
#8192=ORIENTED_EDGE('',*,*,#6306,.T.);
#8193=ORIENTED_EDGE('',*,*,#6308,.F.);
#8194=ORIENTED_EDGE('',*,*,#6309,.F.);
#8195=ORIENTED_EDGE('',*,*,#6310,.T.);
#8196=ORIENTED_EDGE('',*,*,#6307,.T.);
#8197=ORIENTED_EDGE('',*,*,#6310,.F.);
#8198=ORIENTED_EDGE('',*,*,#6311,.F.);
#8199=ORIENTED_EDGE('',*,*,#6312,.T.);
#8200=ORIENTED_EDGE('',*,*,#6309,.T.);
#8201=ORIENTED_EDGE('',*,*,#6312,.F.);
#8202=ORIENTED_EDGE('',*,*,#6311,.T.);
#8203=ORIENTED_EDGE('',*,*,#6313,.F.);
#8204=ORIENTED_EDGE('',*,*,#6314,.F.);
#8205=ORIENTED_EDGE('',*,*,#6315,.T.);
#8206=ORIENTED_EDGE('',*,*,#6313,.T.);
#8207=ORIENTED_EDGE('',*,*,#6315,.F.);
#8208=ORIENTED_EDGE('',*,*,#6305,.T.);
#8209=ORIENTED_EDGE('',*,*,#6316,.T.);
#8210=ORIENTED_EDGE('',*,*,#6314,.T.);
#8211=ORIENTED_EDGE('',*,*,#6316,.F.);
#10325=CYLINDRICAL_SURFACE('',#11708,0.425);
#10326=CYLINDRICAL_SURFACE('',#11716,0.24505);
#10549=ADVANCED_FACE('',(#1207),#641,.F.);
#10550=ADVANCED_FACE('',(#1208),#642,.F.);
#10551=ADVANCED_FACE('',(#1209),#643,.F.);
#10552=ADVANCED_FACE('',(#1210),#644,.F.);
#10553=ADVANCED_FACE('',(#1211),#645,.F.);
#10554=ADVANCED_FACE('',(#1212),#646,.F.);
#10555=ADVANCED_FACE('',(#1213),#647,.F.);
#10556=ADVANCED_FACE('',(#1214),#648,.F.);
#10557=ADVANCED_FACE('',(#1215),#649,.F.);
#10558=ADVANCED_FACE('',(#1216),#650,.T.);
#10559=ADVANCED_FACE('',(#1217),#14,.T.);
#10560=ADVANCED_FACE('',(#1218),#10325,.T.);
#10561=ADVANCED_FACE('',(#1219),#15,.T.);
#10562=ADVANCED_FACE('',(#1220,#482),#651,.T.);
#10563=ADVANCED_FACE('',(#1221),#16,.T.);
#10564=ADVANCED_FACE('',(#1222),#10326,.T.);
#11003=CLOSED_SHELL('',(#10549,#10550,#10551,#10552,#10553,#10554,#10555,
#10556));
#11004=CLOSED_SHELL('',(#10557,#10558,#10559,#10560,#10561,#10562,#10563,
#10564));
#11693=AXIS2_PLACEMENT_3D('',#16720,#13246,#13247);
#11694=AXIS2_PLACEMENT_3D('',#16721,#13248,#13249);
#11695=AXIS2_PLACEMENT_3D('',#16730,#13254,#13255);
#11696=AXIS2_PLACEMENT_3D('',#16736,#13259,#13260);
#11697=AXIS2_PLACEMENT_3D('',#16742,#13264,#13265);
#11698=AXIS2_PLACEMENT_3D('',#16748,#13269,#13270);
#11699=AXIS2_PLACEMENT_3D('',#16754,#13274,#13275);
#11700=AXIS2_PLACEMENT_3D('',#16757,#13278,#13279);
#11701=AXIS2_PLACEMENT_3D('',#16758,#13280,#13281);
#11702=AXIS2_PLACEMENT_3D('',#16759,#13282,#13283);
#11703=AXIS2_PLACEMENT_3D('',#16761,#13284,#13285);
#11704=AXIS2_PLACEMENT_3D('',#16762,#13286,#13287);
#11705=AXIS2_PLACEMENT_3D('',#16764,#13288,#13289);
#11706=AXIS2_PLACEMENT_3D('',#16765,#13290,#13291);
#11707=AXIS2_PLACEMENT_3D('',#16767,#13292,#13293);
#11708=AXIS2_PLACEMENT_3D('',#16769,#13295,#13296);
#11709=AXIS2_PLACEMENT_3D('',#16771,#13297,#13298);
#11710=AXIS2_PLACEMENT_3D('',#16773,#13300,#13301);
#11711=AXIS2_PLACEMENT_3D('',#16775,#13302,#13303);
#11712=AXIS2_PLACEMENT_3D('',#16777,#13305,#13306);
#11713=AXIS2_PLACEMENT_3D('',#16779,#13307,#13308);
#11714=AXIS2_PLACEMENT_3D('',#16780,#13309,#13310);
#11715=AXIS2_PLACEMENT_3D('',#16782,#13311,#13312);
#11716=AXIS2_PLACEMENT_3D('',#16784,#13314,#13315);
#13246=DIRECTION('axis',(0.,0.,1.));
#13247=DIRECTION('refdir',(1.,0.,0.));
#13248=DIRECTION('center_axis',(0.866025403784439,0.,-0.5));
#13249=DIRECTION('ref_axis',(0.5,0.,0.866025403784439));
#13250=DIRECTION('',(-0.5,0.,-0.866025403784439));
#13251=DIRECTION('',(0.,-1.,0.));
#13252=DIRECTION('',(0.5,0.,0.866025403784439));
#13253=DIRECTION('',(0.,-1.,0.));
#13254=DIRECTION('center_axis',(1.20185167898973E-16,0.,-1.));
#13255=DIRECTION('ref_axis',(1.,0.,1.20185167898973E-16));
#13256=DIRECTION('',(-1.,0.,-1.20185167898973E-16));
#13257=DIRECTION('',(0.,-1.,0.));
#13258=DIRECTION('',(1.,0.,1.20185167898973E-16));
#13259=DIRECTION('center_axis',(-0.866025403784439,0.,-0.5));
#13260=DIRECTION('ref_axis',(0.5,0.,-0.866025403784439));
#13261=DIRECTION('',(-0.5,0.,0.866025403784439));
#13262=DIRECTION('',(0.,-1.,0.));
#13263=DIRECTION('',(0.5,0.,-0.866025403784439));
#13264=DIRECTION('center_axis',(-0.866025403784439,0.,0.5));
#13265=DIRECTION('ref_axis',(-0.5,0.,-0.866025403784439));
#13266=DIRECTION('',(0.5,0.,0.866025403784439));
#13267=DIRECTION('',(0.,-1.,0.));
#13268=DIRECTION('',(-0.5,0.,-0.866025403784439));
#13269=DIRECTION('center_axis',(-2.40370335797945E-16,0.,1.));
#13270=DIRECTION('ref_axis',(-1.,0.,-2.40370335797945E-16));
#13271=DIRECTION('',(1.,0.,2.40370335797945E-16));
#13272=DIRECTION('',(0.,-1.,0.));
#13273=DIRECTION('',(-1.,0.,-2.40370335797945E-16));
#13274=DIRECTION('center_axis',(0.866025403784439,0.,0.5));
#13275=DIRECTION('ref_axis',(-0.5,0.,0.866025403784439));
#13276=DIRECTION('',(0.5,0.,-0.866025403784439));
#13277=DIRECTION('',(-0.5,0.,0.866025403784439));
#13278=DIRECTION('center_axis',(0.,1.,0.));
#13279=DIRECTION('ref_axis',(1.,0.,0.));
#13280=DIRECTION('center_axis',(0.,-1.,0.));
#13281=DIRECTION('ref_axis',(0.,0.,-1.));
#13282=DIRECTION('center_axis',(0.,1.,0.));
#13283=DIRECTION('ref_axis',(1.,0.,0.));
#13284=DIRECTION('center_axis',(0.,1.,0.));
#13285=DIRECTION('ref_axis',(1.,0.,0.));
#13286=DIRECTION('center_axis',(0.,1.,0.));
#13287=DIRECTION('ref_axis',(0.,0.,1.));
#13288=DIRECTION('center_axis',(0.,-1.,0.));
#13289=DIRECTION('ref_axis',(1.,0.,0.));
#13290=DIRECTION('center_axis',(0.,-1.,0.));
#13291=DIRECTION('ref_axis',(1.,0.,0.));
#13292=DIRECTION('center_axis',(0.,-1.,0.));
#13293=DIRECTION('ref_axis',(1.,0.,0.));
#13294=DIRECTION('',(0.707106781186548,0.707106781186547,8.65956056235493E-17));
#13295=DIRECTION('center_axis',(0.,-1.,0.));
#13296=DIRECTION('ref_axis',(1.,0.,0.));
#13297=DIRECTION('center_axis',(0.,-1.,0.));
#13298=DIRECTION('ref_axis',(1.,0.,0.));
#13299=DIRECTION('',(0.,1.,0.));
#13300=DIRECTION('center_axis',(0.,1.,0.));
#13301=DIRECTION('ref_axis',(1.,0.,0.));
#13302=DIRECTION('center_axis',(0.,-1.,0.));
#13303=DIRECTION('ref_axis',(1.,0.,0.));
#13304=DIRECTION('',(-0.707106781186547,0.707106781186548,-8.65956056235493E-17));
#13305=DIRECTION('center_axis',(0.,-1.,0.));
#13306=DIRECTION('ref_axis',(0.,0.,-1.));
#13307=DIRECTION('center_axis',(0.,-1.,0.));
#13308=DIRECTION('ref_axis',(1.,0.,0.));
#13309=DIRECTION('center_axis',(0.,1.,0.));
#13310=DIRECTION('ref_axis',(1.,0.,0.));
#13311=DIRECTION('center_axis',(0.,1.,0.));
#13312=DIRECTION('ref_axis',(1.,0.,0.));
#13313=DIRECTION('',(-0.447213595499958,0.894427190999916,-5.47678698264203E-17));
#13314=DIRECTION('center_axis',(0.,-1.,0.));
#13315=DIRECTION('ref_axis',(1.,0.,0.));
#13316=DIRECTION('',(0.,1.,0.));
#16720=CARTESIAN_POINT('',(0.,0.,0.));
#16721=CARTESIAN_POINT('Origin',(0.115470053837925,-0.5,-0.2));
#16722=CARTESIAN_POINT('',(0.23094010767585,-0.5,0.));
#16723=CARTESIAN_POINT('',(0.115470053837925,-0.5,-0.2));
#16724=CARTESIAN_POINT('',(0.23094010767585,-0.5,0.));
#16725=CARTESIAN_POINT('',(0.115470053837925,-0.8,-0.2));
#16726=CARTESIAN_POINT('',(0.115470053837925,-0.5,-0.2));
#16727=CARTESIAN_POINT('',(0.23094010767585,-0.8,0.));
#16728=CARTESIAN_POINT('',(0.23094010767585,-0.8,0.));
#16729=CARTESIAN_POINT('',(0.23094010767585,-0.5,0.));
#16730=CARTESIAN_POINT('Origin',(-0.115470053837925,-0.5,-0.2));
#16731=CARTESIAN_POINT('',(-0.115470053837925,-0.5,-0.2));
#16732=CARTESIAN_POINT('',(0.115470053837925,-0.5,-0.2));
#16733=CARTESIAN_POINT('',(-0.115470053837925,-0.8,-0.2));
#16734=CARTESIAN_POINT('',(-0.115470053837925,-0.5,-0.2));
#16735=CARTESIAN_POINT('',(0.115470053837925,-0.8,-0.2));
#16736=CARTESIAN_POINT('Origin',(-0.23094010767585,-0.5,-2.77555756156289E-17));
#16737=CARTESIAN_POINT('',(-0.23094010767585,-0.5,-2.82820063659975E-17));
#16738=CARTESIAN_POINT('',(-0.115470053837925,-0.5,-0.2));
#16739=CARTESIAN_POINT('',(-0.23094010767585,-0.8,-2.77555756156289E-17));
#16740=CARTESIAN_POINT('',(-0.23094010767585,-0.5,-2.82820063659975E-17));
#16741=CARTESIAN_POINT('',(-0.115470053837925,-0.8,-0.2));
#16742=CARTESIAN_POINT('Origin',(-0.115470053837925,-0.5,0.2));
#16743=CARTESIAN_POINT('',(-0.115470053837925,-0.5,0.2));
#16744=CARTESIAN_POINT('',(-0.23094010767585,-0.5,-2.82820063659975E-17));
#16745=CARTESIAN_POINT('',(-0.115470053837925,-0.8,0.2));
#16746=CARTESIAN_POINT('',(-0.115470053837925,-0.5,0.2));
#16747=CARTESIAN_POINT('',(-0.23094010767585,-0.8,-2.82820063659975E-17));
#16748=CARTESIAN_POINT('Origin',(0.115470053837925,-0.5,0.2));
#16749=CARTESIAN_POINT('',(0.115470053837925,-0.5,0.2));
#16750=CARTESIAN_POINT('',(-0.115470053837925,-0.5,0.2));
#16751=CARTESIAN_POINT('',(0.115470053837925,-0.8,0.2));
#16752=CARTESIAN_POINT('',(0.115470053837925,-0.5,0.2));
#16753=CARTESIAN_POINT('',(-0.115470053837925,-0.8,0.2));
#16754=CARTESIAN_POINT('Origin',(0.23094010767585,-0.5,0.));
#16755=CARTESIAN_POINT('',(0.115470053837925,-0.5,0.2));
#16756=CARTESIAN_POINT('',(0.115470053837925,-0.8,0.2));
#16757=CARTESIAN_POINT('Origin',(0.,-0.5,0.));
#16758=CARTESIAN_POINT('Origin',(0.,-0.8,0.));
#16759=CARTESIAN_POINT('Origin',(0.,-1.4,0.));
#16760=CARTESIAN_POINT('',(-0.24505,-1.4,3.00099698131059E-17));
#16761=CARTESIAN_POINT('Origin',(0.,-1.4,0.));
#16762=CARTESIAN_POINT('Origin',(0.375,0.5,0.));
#16763=CARTESIAN_POINT('',(-0.375,0.5,-4.59242549680257E-17));
#16764=CARTESIAN_POINT('Origin',(0.,0.5,0.));
#16765=CARTESIAN_POINT('Origin',(0.,0.475,0.));
#16766=CARTESIAN_POINT('',(-0.425,0.45,-5.20474889637625E-17));
#16767=CARTESIAN_POINT('Origin',(0.,0.45,0.));
#16768=CARTESIAN_POINT('',(-0.4,0.475,-4.89858719658941E-17));
#16769=CARTESIAN_POINT('Origin',(0.,0.24,0.));
#16770=CARTESIAN_POINT('',(-0.425,0.0299999999999998,-5.20474889637625E-17));
#16771=CARTESIAN_POINT('Origin',(0.,0.0299999999999998,0.));
#16772=CARTESIAN_POINT('',(-0.425,0.24,-5.20474889637625E-17));
#16773=CARTESIAN_POINT('Origin',(0.,0.0150000000000001,0.));
#16774=CARTESIAN_POINT('',(-0.395,4.85722573273506E-17,-4.83735485663204E-17));
#16775=CARTESIAN_POINT('Origin',(0.,0.,0.));
#16776=CARTESIAN_POINT('',(-0.41,0.0150000000000001,-5.02105187650415E-17));
#16777=CARTESIAN_POINT('Origin',(0.27,0.,0.));
#16778=CARTESIAN_POINT('',(-0.27,0.,-3.30654635769785E-17));
#16779=CARTESIAN_POINT('Origin',(0.,0.,0.));
#16780=CARTESIAN_POINT('Origin',(0.,-0.02,0.));
#16781=CARTESIAN_POINT('',(-0.24505,-0.0498999999999999,3.00099698131059E-17));
#16782=CARTESIAN_POINT('Origin',(0.,-0.0498999999999999,0.));
#16783=CARTESIAN_POINT('',(-0.26,-0.02,-3.18408167778312E-17));
#16784=CARTESIAN_POINT('Origin',(0.,-0.995,0.));
#16785=CARTESIAN_POINT('',(-0.24505,-0.995,-3.00099698131059E-17));
#19306=UNCERTAINTY_MEASURE_WITH_UNIT(LENGTH_MEASURE(0.001),#19362,
'DISTANCE_ACCURACY_VALUE',
'Maximum model space distance between geometric entities at asserted c
onnectivities');
#19323=UNCERTAINTY_MEASURE_WITH_UNIT(LENGTH_MEASURE(0.001),#19362,
'DISTANCE_ACCURACY_VALUE',
'Maximum model space distance between geometric entities at asserted c
onnectivities');
#19344=(
GEOMETRIC_REPRESENTATION_CONTEXT(3)
GLOBAL_UNCERTAINTY_ASSIGNED_CONTEXT((#19306))
GLOBAL_UNIT_ASSIGNED_CONTEXT((#19362,#19364,#19365))
REPRESENTATION_CONTEXT('','3D')
);
#19361=(
GEOMETRIC_REPRESENTATION_CONTEXT(3)
GLOBAL_UNCERTAINTY_ASSIGNED_CONTEXT((#19323))
GLOBAL_UNIT_ASSIGNED_CONTEXT((#19362,#19364,#19365))
REPRESENTATION_CONTEXT('','3D')
);
#19362=(
LENGTH_UNIT()
NAMED_UNIT(*)
SI_UNIT(.CENTI.,.METRE.)
);
#19364=(
NAMED_UNIT(*)
PLANE_ANGLE_UNIT()
SI_UNIT($,.RADIAN.)
);
#19365=(
NAMED_UNIT(*)
SI_UNIT($,.STERADIAN.)
SOLID_ANGLE_UNIT()
);
#19386=SHAPE_DEFINITION_REPRESENTATION(#19425,#19508);
#19425=PRODUCT_DEFINITION_SHAPE('',$,#19546);
#19508=SHAPE_REPRESENTATION('',(#11693),#19344);
#19525=PRODUCT_DEFINITION_CONTEXT('part definition',#19638,'design');
#19546=PRODUCT_DEFINITION('M5x14 Cap Screw','M5x14 Cap Screw',#19583,#19525);
#19583=PRODUCT_DEFINITION_FORMATION('',$,#19660);
#19638=APPLICATION_CONTEXT(
'Core Data for Automotive Mechanical Design Process');
#19639=PRODUCT_CONTEXT('part definition',#19638,'mechanical');
#19660=PRODUCT('M5x14 Cap Screw','M5x14 Cap Screw','M5x14 Cap Screw',(#19639));
#19747=COLOUR_RGB('Black',0.12,0.14,0.17);
#19748=FILL_AREA_STYLE_COLOUR('',#19747);
#19749=FILL_AREA_STYLE('',(#19748));
#19750=SURFACE_STYLE_FILL_AREA(#19749);
#19751=SURFACE_SIDE_STYLE('',(#19750));
#19752=SURFACE_STYLE_USAGE(.BOTH.,#19751);
#19753=PRESENTATION_STYLE_ASSIGNMENT((#19752));
ENDSEC;
END-ISO-10303-21;
